ISO-10303-21;
HEADER;
/* Generated by software containing ST-Developer
 * from STEP Tools, Inc. (www.steptools.com) 
 */

FILE_DESCRIPTION(
/* description */ ('Four-bar parallelogram arm'),
/* implementation_level */ '2;1');

FILE_NAME(
/* name */ 'Inner race sleeve (1).step',
/* time_stamp */ '2026-10-28T03:24:55-07:00',
/* author */ (''),
/* organization */ (''),
/* preprocessor_version */ 'ST-DEVELOPER v20.2',
/* originating_system */ 'Autodesk Translation Framework v15.17.0.0',
/* authorisation */ '');

FILE_SCHEMA (('AUTOMOTIVE_DESIGN { 1 0 10303 214 3 1 1 }'));
ENDSEC;

DATA;
#10=MECHANICAL_DESIGN_GEOMETRIC_PRESENTATION_REPRESENTATION('',(#632),#14512);
#532=SHAPE_REPRESENTATION_RELATIONSHIP('SRR','None',#14753,#582);
#582=ADVANCED_BREP_SHAPE_REPRESENTATION('',(#690),#14468);
#632=STYLED_ITEM('',(#15087),#690);
#690=MANIFOLD_SOLID_BREP('Body1',#7336);
#794=FACE_BOUND('',#1769,.T.);
#795=FACE_BOUND('',#1771,.T.);
#1053=PLANE('',#8121);
#1054=PLANE('',#8122);
#1287=FACE_OUTER_BOUND('',#1766,.T.);
#1288=FACE_OUTER_BOUND('',#1767,.T.);
#1289=FACE_OUTER_BOUND('',#1768,.T.);
#1290=FACE_OUTER_BOUND('',#1770,.T.);
#1766=EDGE_LOOP('',(#5342,#5343,#5344,#5345));
#1767=EDGE_LOOP('',(#5346,#5347,#5348,#5349));
#1768=EDGE_LOOP('',(#5350));
#1769=EDGE_LOOP('',(#5351));
#1770=EDGE_LOOP('',(#5352));
#1771=EDGE_LOOP('',(#5353));
#2411=LINE('',#11826,#2805);
#2412=LINE('',#11832,#2806);
#2805=VECTOR('',#9427,0.505);
#2806=VECTOR('',#9434,0.7);
#3178=CIRCLE('',#8116,0.505);
#3179=CIRCLE('',#8117,0.505);
#3180=CIRCLE('',#8119,0.7);
#3181=CIRCLE('',#8120,0.7);
#3663=VERTEX_POINT('',#11823);
#3664=VERTEX_POINT('',#11825);
#3665=VERTEX_POINT('',#11829);
#3666=VERTEX_POINT('',#11831);
#4302=EDGE_CURVE('',#3663,#3663,#3178,.T.);
#4303=EDGE_CURVE('',#3663,#3664,#2411,.T.);
#4304=EDGE_CURVE('',#3664,#3664,#3179,.T.);
#4305=EDGE_CURVE('',#3665,#3665,#3180,.T.);
#4306=EDGE_CURVE('',#3665,#3666,#2412,.T.);
#4307=EDGE_CURVE('',#3666,#3666,#3181,.T.);
#5342=ORIENTED_EDGE('',*,*,#4302,.F.);
#5343=ORIENTED_EDGE('',*,*,#4303,.T.);
#5344=ORIENTED_EDGE('',*,*,#4304,.T.);
#5345=ORIENTED_EDGE('',*,*,#4303,.F.);
#5346=ORIENTED_EDGE('',*,*,#4305,.F.);
#5347=ORIENTED_EDGE('',*,*,#4306,.T.);
#5348=ORIENTED_EDGE('',*,*,#4307,.T.);
#5349=ORIENTED_EDGE('',*,*,#4306,.F.);
#5350=ORIENTED_EDGE('',*,*,#4305,.T.);
#5351=ORIENTED_EDGE('',*,*,#4302,.T.);
#5352=ORIENTED_EDGE('',*,*,#4307,.F.);
#5353=ORIENTED_EDGE('',*,*,#4304,.F.);
#6753=CYLINDRICAL_SURFACE('',#8115,0.505);
#6754=CYLINDRICAL_SURFACE('',#8118,0.7);
#6992=ADVANCED_FACE('',(#1287),#6753,.F.);
#6993=ADVANCED_FACE('',(#1288),#6754,.T.);
#6994=ADVANCED_FACE('',(#1289,#794),#1053,.T.);
#6995=ADVANCED_FACE('',(#1290,#795),#1054,.F.);
#7336=CLOSED_SHELL('',(#6992,#6993,#6994,#6995));
#8114=AXIS2_PLACEMENT_3D('',#11821,#9421,#9422);
#8115=AXIS2_PLACEMENT_3D('',#11822,#9423,#9424);
#8116=AXIS2_PLACEMENT_3D('',#11824,#9425,#9426);
#8117=AXIS2_PLACEMENT_3D('',#11827,#9428,#9429);
#8118=AXIS2_PLACEMENT_3D('',#11828,#9430,#9431);
#8119=AXIS2_PLACEMENT_3D('',#11830,#9432,#9433);
#8120=AXIS2_PLACEMENT_3D('',#11833,#9435,#9436);
#8121=AXIS2_PLACEMENT_3D('',#11834,#9437,#9438);
#8122=AXIS2_PLACEMENT_3D('',#11835,#9439,#9440);
#9421=DIRECTION('axis',(0.,0.,1.));
#9422=DIRECTION('refdir',(1.,0.,0.));
#9423=DIRECTION('center_axis',(0.,1.,0.));
#9424=DIRECTION('ref_axis',(1.,0.,0.));
#9425=DIRECTION('center_axis',(0.,-1.,0.));
#9426=DIRECTION('ref_axis',(1.,0.,0.));
#9427=DIRECTION('',(0.,-1.,0.));
#9428=DIRECTION('center_axis',(0.,-1.,0.));
#9429=DIRECTION('ref_axis',(1.,0.,0.));
#9430=DIRECTION('center_axis',(0.,1.,0.));
#9431=DIRECTION('ref_axis',(1.,0.,0.));
#9432=DIRECTION('center_axis',(0.,1.,0.));
#9433=DIRECTION('ref_axis',(1.,0.,0.));
#9434=DIRECTION('',(0.,-1.,0.));
#9435=DIRECTION('center_axis',(0.,1.,0.));
#9436=DIRECTION('ref_axis',(1.,0.,0.));
#9437=DIRECTION('center_axis',(0.,1.,0.));
#9438=DIRECTION('ref_axis',(1.,0.,0.));
#9439=DIRECTION('center_axis',(0.,1.,0.));
#9440=DIRECTION('ref_axis',(1.,0.,0.));
#11821=CARTESIAN_POINT('',(0.,0.,0.));
#11822=CARTESIAN_POINT('Origin',(0.,-0.15,14.));
#11823=CARTESIAN_POINT('',(-0.505,0.15,14.));
#11824=CARTESIAN_POINT('Origin',(0.,0.15,14.));
#11825=CARTESIAN_POINT('',(-0.505,-0.15,14.));
#11826=CARTESIAN_POINT('',(-0.505,-0.15,14.));
#11827=CARTESIAN_POINT('Origin',(0.,-0.15,14.));
#11828=CARTESIAN_POINT('Origin',(0.,-0.15,14.));
#11829=CARTESIAN_POINT('',(-0.7,0.15,14.));
#11830=CARTESIAN_POINT('Origin',(0.,0.15,14.));
#11831=CARTESIAN_POINT('',(-0.7,-0.15,14.));
#11832=CARTESIAN_POINT('',(-0.7,-0.15,14.));
#11833=CARTESIAN_POINT('Origin',(0.,-0.15,14.));
#11834=CARTESIAN_POINT('Origin',(0.,0.15,14.));
#11835=CARTESIAN_POINT('Origin',(0.,-0.15,14.));
#14411=UNCERTAINTY_MEASURE_WITH_UNIT(LENGTH_MEASURE(0.001),#14513,
'DISTANCE_ACCURACY_VALUE',
'Maximum model space distance between geometric entities at asserted c
onnectivities');
#14455=UNCERTAINTY_MEASURE_WITH_UNIT(LENGTH_MEASURE(0.001),#14513,
'DISTANCE_ACCURACY_VALUE',
'Maximum model space distance between geometric entities at asserted c
onnectivities');
#14468=(
GEOMETRIC_REPRESENTATION_CONTEXT(3)
GLOBAL_UNCERTAINTY_ASSIGNED_CONTEXT((#14411))
GLOBAL_UNIT_ASSIGNED_CONTEXT((#14513,#14515,#14516))
REPRESENTATION_CONTEXT('','3D')
);
#14512=(
GEOMETRIC_REPRESENTATION_CONTEXT(3)
GLOBAL_UNCERTAINTY_ASSIGNED_CONTEXT((#14455))
GLOBAL_UNIT_ASSIGNED_CONTEXT((#14513,#14515,#14516))
REPRESENTATION_CONTEXT('','3D')
);
#14513=(
LENGTH_UNIT()
NAMED_UNIT(*)
SI_UNIT(.CENTI.,.METRE.)
);
#14515=(
NAMED_UNIT(*)
PLANE_ANGLE_UNIT()
SI_UNIT($,.RADIAN.)
);
#14516=(
NAMED_UNIT(*)
SI_UNIT($,.STERADIAN.)
SOLID_ANGLE_UNIT()
);
#14529=SHAPE_DEFINITION_REPRESENTATION(#14585,#14753);
#14585=PRODUCT_DEFINITION_SHAPE('',$,#14810);
#14753=SHAPE_REPRESENTATION('',(#8114),#14468);
#14797=PRODUCT_DEFINITION_CONTEXT('part definition',#14967,'design');
#14810=PRODUCT_DEFINITION('Inner race sleeve (1)','Inner race sleeve (1)',
#14866,#14797);
#14866=PRODUCT_DEFINITION_FORMATION('',$,#14981);
#14967=APPLICATION_CONTEXT(
'Core Data for Automotive Mechanical Design Process');
#14968=PRODUCT_CONTEXT('part definition',#14967,'mechanical');
#14981=PRODUCT('Inner race sleeve (1)','Inner race sleeve (1)',
'Inner race sleeve (1)',(#14968));
#15081=COLOUR_RGB('Grey',0.48,0.52,0.57);
#15082=FILL_AREA_STYLE_COLOUR('',#15081);
#15083=FILL_AREA_STYLE('',(#15082));
#15084=SURFACE_STYLE_FILL_AREA(#15083);
#15085=SURFACE_SIDE_STYLE('',(#15084));
#15086=SURFACE_STYLE_USAGE(.BOTH.,#15085);
#15087=PRESENTATION_STYLE_ASSIGNMENT((#15086));
ENDSEC;
END-ISO-10303-21;
